ISO-10303-21;
HEADER;
/* Generated by software containing ST-Developer
 * from STEP Tools, Inc. (www.steptools.com) 
 */

FILE_DESCRIPTION(
/* description */ (''),
/* implementation_level */ '2;1');

FILE_NAME(
/* name */ 'M5x14 Cap Screw (1).step',
/* time_stamp */ '2026-10-29T16:43:51-07:00',
/* author */ (''),
/* organization */ (''),
/* preprocessor_version */ 'ST-DEVELOPER v20.2',
/* originating_system */ 'Autodesk Translation Framework v15.17.0.0',
/* authorisation */ '');

FILE_SCHEMA (('AUTOMOTIVE_DESIGN { 1 0 10303 214 3 1 1 }'));
ENDSEC;

DATA;
#10=MECHANICAL_DESIGN_GEOMETRIC_PRESENTATION_REPRESENTATION('',(#372),#10292);
#284=ORIENTED_CLOSED_SHELL('',*,#5015,.F.);
#289=BREP_WITH_VOIDS('Body1',#5016,(#284));
#298=CONICAL_SURFACE('',#5486,0.4,0.785398163397448);
#299=CONICAL_SURFACE('',#5490,0.41,0.785398163397448);
#300=CONICAL_SURFACE('',#5494,0.26,0.463647609000806);
#326=SHAPE_REPRESENTATION_RELATIONSHIP('SRR','None',#10422,#349);
#349=ADVANCED_BREP_SHAPE_REPRESENTATION('',(#289),#10274);
#372=STYLED_ITEM('',(#10635),#289);
#466=FACE_BOUND('',#1172,.T.);
#591=PLANE('',#5474);
#592=PLANE('',#5475);
#593=PLANE('',#5476);
#594=PLANE('',#5477);
#595=PLANE('',#5478);
#596=PLANE('',#5479);
#597=PLANE('',#5480);
#598=PLANE('',#5481);
#599=PLANE('',#5482);
#600=PLANE('',#5484);
#601=PLANE('',#5492);
#810=FACE_OUTER_BOUND('',#1158,.T.);
#811=FACE_OUTER_BOUND('',#1159,.T.);
#812=FACE_OUTER_BOUND('',#1160,.T.);
#813=FACE_OUTER_BOUND('',#1161,.T.);
#814=FACE_OUTER_BOUND('',#1162,.T.);
#815=FACE_OUTER_BOUND('',#1163,.T.);
#816=FACE_OUTER_BOUND('',#1164,.T.);
#817=FACE_OUTER_BOUND('',#1165,.T.);
#818=FACE_OUTER_BOUND('',#1166,.T.);
#819=FACE_OUTER_BOUND('',#1167,.T.);
#820=FACE_OUTER_BOUND('',#1168,.T.);
#821=FACE_OUTER_BOUND('',#1169,.T.);
#822=FACE_OUTER_BOUND('',#1170,.T.);
#823=FACE_OUTER_BOUND('',#1171,.T.);
#824=FACE_OUTER_BOUND('',#1173,.T.);
#825=FACE_OUTER_BOUND('',#1174,.T.);
#1158=EDGE_LOOP('',(#3879,#3880,#3881,#3882));
#1159=EDGE_LOOP('',(#3883,#3884,#3885,#3886));
#1160=EDGE_LOOP('',(#3887,#3888,#3889,#3890));
#1161=EDGE_LOOP('',(#3891,#3892,#3893,#3894));
#1162=EDGE_LOOP('',(#3895,#3896,#3897,#3898));
#1163=EDGE_LOOP('',(#3899,#3900,#3901,#3902));
#1164=EDGE_LOOP('',(#3903,#3904,#3905,#3906,#3907,#3908));
#1165=EDGE_LOOP('',(#3909,#3910,#3911,#3912,#3913,#3914));
#1166=EDGE_LOOP('',(#3915));
#1167=EDGE_LOOP('',(#3916));
#1168=EDGE_LOOP('',(#3917,#3918,#3919,#3920));
#1169=EDGE_LOOP('',(#3921,#3922,#3923,#3924));
#1170=EDGE_LOOP('',(#3925,#3926,#3927,#3928));
#1171=EDGE_LOOP('',(#3929));
#1172=EDGE_LOOP('',(#3930));
#1173=EDGE_LOOP('',(#3931,#3932,#3933,#3934));
#1174=EDGE_LOOP('',(#3935,#3936,#3937,#3938));
#1571=LINE('',#7909,#1963);
#1572=LINE('',#7911,#1964);
#1573=LINE('',#7913,#1965);
#1574=LINE('',#7914,#1966);
#1575=LINE('',#7917,#1967);
#1576=LINE('',#7919,#1968);
#1577=LINE('',#7920,#1969);
#1578=LINE('',#7923,#1970);
#1579=LINE('',#7925,#1971);
#1580=LINE('',#7926,#1972);
#1581=LINE('',#7929,#1973);
#1582=LINE('',#7931,#1974);
#1583=LINE('',#7932,#1975);
#1584=LINE('',#7935,#1976);
#1585=LINE('',#7937,#1977);
#1586=LINE('',#7938,#1978);
#1587=LINE('',#7940,#1979);
#1588=LINE('',#7941,#1980);
#1589=LINE('',#7953,#1981);
#1590=LINE('',#7957,#1982);
#1591=LINE('',#7961,#1983);
#1592=LINE('',#7968,#1984);
#1593=LINE('',#7970,#1985);
#1963=VECTOR('',#6396,1.);
#1964=VECTOR('',#6397,1.);
#1965=VECTOR('',#6398,1.);
#1966=VECTOR('',#6399,1.);
#1967=VECTOR('',#6402,1.);
#1968=VECTOR('',#6403,1.);
#1969=VECTOR('',#6404,1.);
#1970=VECTOR('',#6407,1.);
#1971=VECTOR('',#6408,1.);
#1972=VECTOR('',#6409,1.);
#1973=VECTOR('',#6412,1.);
#1974=VECTOR('',#6413,1.);
#1975=VECTOR('',#6414,1.);
#1976=VECTOR('',#6417,1.);
#1977=VECTOR('',#6418,1.);
#1978=VECTOR('',#6419,1.);
#1979=VECTOR('',#6422,1.);
#1980=VECTOR('',#6423,1.);
#1981=VECTOR('',#6440,0.4);
#1982=VECTOR('',#6445,0.425);
#1983=VECTOR('',#6450,0.41);
#1984=VECTOR('',#6459,0.26);
#1985=VECTOR('',#6462,0.25);
#2270=CIRCLE('',#5483,0.24505);
#2271=CIRCLE('',#5485,0.375);
#2272=CIRCLE('',#5487,0.425);
#2273=CIRCLE('',#5489,0.425);
#2274=CIRCLE('',#5491,0.395);
#2275=CIRCLE('',#5493,0.27);
#2276=CIRCLE('',#5495,0.24505);
#2549=VERTEX_POINT('',#7907);
#2550=VERTEX_POINT('',#7908);
#2551=VERTEX_POINT('',#7910);
#2552=VERTEX_POINT('',#7912);
#2553=VERTEX_POINT('',#7916);
#2554=VERTEX_POINT('',#7918);
#2555=VERTEX_POINT('',#7922);
#2556=VERTEX_POINT('',#7924);
#2557=VERTEX_POINT('',#7928);
#2558=VERTEX_POINT('',#7930);
#2559=VERTEX_POINT('',#7934);
#2560=VERTEX_POINT('',#7936);
#2561=VERTEX_POINT('',#7945);
#2562=VERTEX_POINT('',#7948);
#2563=VERTEX_POINT('',#7951);
#2564=VERTEX_POINT('',#7955);
#2565=VERTEX_POINT('',#7959);
#2566=VERTEX_POINT('',#7963);
#2567=VERTEX_POINT('',#7966);
#3030=EDGE_CURVE('',#2549,#2550,#1571,.T.);
#3031=EDGE_CURVE('',#2550,#2551,#1572,.T.);
#3032=EDGE_CURVE('',#2551,#2552,#1573,.T.);
#3033=EDGE_CURVE('',#2549,#2552,#1574,.T.);
#3034=EDGE_CURVE('',#2550,#2553,#1575,.T.);
#3035=EDGE_CURVE('',#2553,#2554,#1576,.T.);
#3036=EDGE_CURVE('',#2554,#2551,#1577,.T.);
#3037=EDGE_CURVE('',#2553,#2555,#1578,.T.);
#3038=EDGE_CURVE('',#2555,#2556,#1579,.T.);
#3039=EDGE_CURVE('',#2556,#2554,#1580,.T.);
#3040=EDGE_CURVE('',#2555,#2557,#1581,.T.);
#3041=EDGE_CURVE('',#2557,#2558,#1582,.T.);
#3042=EDGE_CURVE('',#2558,#2556,#1583,.T.);
#3043=EDGE_CURVE('',#2557,#2559,#1584,.T.);
#3044=EDGE_CURVE('',#2559,#2560,#1585,.T.);
#3045=EDGE_CURVE('',#2560,#2558,#1586,.T.);
#3046=EDGE_CURVE('',#2559,#2549,#1587,.T.);
#3047=EDGE_CURVE('',#2552,#2560,#1588,.T.);
#3048=EDGE_CURVE('',#2561,#2561,#2270,.T.);
#3049=EDGE_CURVE('',#2562,#2562,#2271,.T.);
#3050=EDGE_CURVE('',#2563,#2563,#2272,.T.);
#3051=EDGE_CURVE('',#2563,#2562,#1589,.T.);
#3052=EDGE_CURVE('',#2564,#2564,#2273,.T.);
#3053=EDGE_CURVE('',#2564,#2563,#1590,.T.);
#3054=EDGE_CURVE('',#2565,#2565,#2274,.T.);
#3055=EDGE_CURVE('',#2565,#2564,#1591,.T.);
#3056=EDGE_CURVE('',#2566,#2566,#2275,.T.);
#3057=EDGE_CURVE('',#2567,#2567,#2276,.F.);
#3058=EDGE_CURVE('',#2567,#2566,#1592,.T.);
#3059=EDGE_CURVE('',#2561,#2567,#1593,.T.);
#3879=ORIENTED_EDGE('',*,*,#3030,.T.);
#3880=ORIENTED_EDGE('',*,*,#3031,.T.);
#3881=ORIENTED_EDGE('',*,*,#3032,.T.);
#3882=ORIENTED_EDGE('',*,*,#3033,.F.);
#3883=ORIENTED_EDGE('',*,*,#3034,.T.);
#3884=ORIENTED_EDGE('',*,*,#3035,.T.);
#3885=ORIENTED_EDGE('',*,*,#3036,.T.);
#3886=ORIENTED_EDGE('',*,*,#3031,.F.);
#3887=ORIENTED_EDGE('',*,*,#3037,.T.);
#3888=ORIENTED_EDGE('',*,*,#3038,.T.);
#3889=ORIENTED_EDGE('',*,*,#3039,.T.);
#3890=ORIENTED_EDGE('',*,*,#3035,.F.);
#3891=ORIENTED_EDGE('',*,*,#3040,.T.);
#3892=ORIENTED_EDGE('',*,*,#3041,.T.);
#3893=ORIENTED_EDGE('',*,*,#3042,.T.);
#3894=ORIENTED_EDGE('',*,*,#3038,.F.);
#3895=ORIENTED_EDGE('',*,*,#3043,.T.);
#3896=ORIENTED_EDGE('',*,*,#3044,.T.);
#3897=ORIENTED_EDGE('',*,*,#3045,.T.);
#3898=ORIENTED_EDGE('',*,*,#3041,.F.);
#3899=ORIENTED_EDGE('',*,*,#3046,.T.);
#3900=ORIENTED_EDGE('',*,*,#3033,.T.);
#3901=ORIENTED_EDGE('',*,*,#3047,.T.);
#3902=ORIENTED_EDGE('',*,*,#3044,.F.);
#3903=ORIENTED_EDGE('',*,*,#3046,.F.);
#3904=ORIENTED_EDGE('',*,*,#3043,.F.);
#3905=ORIENTED_EDGE('',*,*,#3040,.F.);
#3906=ORIENTED_EDGE('',*,*,#3037,.F.);
#3907=ORIENTED_EDGE('',*,*,#3034,.F.);
#3908=ORIENTED_EDGE('',*,*,#3030,.F.);
#3909=ORIENTED_EDGE('',*,*,#3047,.F.);
#3910=ORIENTED_EDGE('',*,*,#3032,.F.);
#3911=ORIENTED_EDGE('',*,*,#3036,.F.);
#3912=ORIENTED_EDGE('',*,*,#3039,.F.);
#3913=ORIENTED_EDGE('',*,*,#3042,.F.);
#3914=ORIENTED_EDGE('',*,*,#3045,.F.);
#3915=ORIENTED_EDGE('',*,*,#3048,.F.);
#3916=ORIENTED_EDGE('',*,*,#3049,.F.);
#3917=ORIENTED_EDGE('',*,*,#3050,.F.);
#3918=ORIENTED_EDGE('',*,*,#3051,.T.);
#3919=ORIENTED_EDGE('',*,*,#3049,.T.);
#3920=ORIENTED_EDGE('',*,*,#3051,.F.);
#3921=ORIENTED_EDGE('',*,*,#3052,.F.);
#3922=ORIENTED_EDGE('',*,*,#3053,.T.);
#3923=ORIENTED_EDGE('',*,*,#3050,.T.);
#3924=ORIENTED_EDGE('',*,*,#3053,.F.);
#3925=ORIENTED_EDGE('',*,*,#3054,.F.);
#3926=ORIENTED_EDGE('',*,*,#3055,.T.);
#3927=ORIENTED_EDGE('',*,*,#3052,.T.);
#3928=ORIENTED_EDGE('',*,*,#3055,.F.);
#3929=ORIENTED_EDGE('',*,*,#3054,.T.);
#3930=ORIENTED_EDGE('',*,*,#3056,.F.);
#3931=ORIENTED_EDGE('',*,*,#3057,.F.);
#3932=ORIENTED_EDGE('',*,*,#3058,.T.);
#3933=ORIENTED_EDGE('',*,*,#3056,.T.);
#3934=ORIENTED_EDGE('',*,*,#3058,.F.);
#3935=ORIENTED_EDGE('',*,*,#3048,.T.);
#3936=ORIENTED_EDGE('',*,*,#3059,.T.);
#3937=ORIENTED_EDGE('',*,*,#3057,.T.);
#3938=ORIENTED_EDGE('',*,*,#3059,.F.);
#4672=CYLINDRICAL_SURFACE('',#5488,0.425);
#4673=CYLINDRICAL_SURFACE('',#5496,0.24505);
#4819=ADVANCED_FACE('',(#810),#591,.F.);
#4820=ADVANCED_FACE('',(#811),#592,.F.);
#4821=ADVANCED_FACE('',(#812),#593,.F.);
#4822=ADVANCED_FACE('',(#813),#594,.F.);
#4823=ADVANCED_FACE('',(#814),#595,.F.);
#4824=ADVANCED_FACE('',(#815),#596,.F.);
#4825=ADVANCED_FACE('',(#816),#597,.F.);
#4826=ADVANCED_FACE('',(#817),#598,.F.);
#4827=ADVANCED_FACE('',(#818),#599,.F.);
#4828=ADVANCED_FACE('',(#819),#600,.T.);
#4829=ADVANCED_FACE('',(#820),#298,.T.);
#4830=ADVANCED_FACE('',(#821),#4672,.T.);
#4831=ADVANCED_FACE('',(#822),#299,.T.);
#4832=ADVANCED_FACE('',(#823,#466),#601,.T.);
#4833=ADVANCED_FACE('',(#824),#300,.T.);
#4834=ADVANCED_FACE('',(#825),#4673,.T.);
#5015=CLOSED_SHELL('',(#4819,#4820,#4821,#4822,#4823,#4824,#4825,#4826));
#5016=CLOSED_SHELL('',(#4827,#4828,#4829,#4830,#4831,#4832,#4833,#4834));
#5473=AXIS2_PLACEMENT_3D('',#7905,#6392,#6393);
#5474=AXIS2_PLACEMENT_3D('',#7906,#6394,#6395);
#5475=AXIS2_PLACEMENT_3D('',#7915,#6400,#6401);
#5476=AXIS2_PLACEMENT_3D('',#7921,#6405,#6406);
#5477=AXIS2_PLACEMENT_3D('',#7927,#6410,#6411);
#5478=AXIS2_PLACEMENT_3D('',#7933,#6415,#6416);
#5479=AXIS2_PLACEMENT_3D('',#7939,#6420,#6421);
#5480=AXIS2_PLACEMENT_3D('',#7942,#6424,#6425);
#5481=AXIS2_PLACEMENT_3D('',#7943,#6426,#6427);
#5482=AXIS2_PLACEMENT_3D('',#7944,#6428,#6429);
#5483=AXIS2_PLACEMENT_3D('',#7946,#6430,#6431);
#5484=AXIS2_PLACEMENT_3D('',#7947,#6432,#6433);
#5485=AXIS2_PLACEMENT_3D('',#7949,#6434,#6435);
#5486=AXIS2_PLACEMENT_3D('',#7950,#6436,#6437);
#5487=AXIS2_PLACEMENT_3D('',#7952,#6438,#6439);
#5488=AXIS2_PLACEMENT_3D('',#7954,#6441,#6442);
#5489=AXIS2_PLACEMENT_3D('',#7956,#6443,#6444);
#5490=AXIS2_PLACEMENT_3D('',#7958,#6446,#6447);
#5491=AXIS2_PLACEMENT_3D('',#7960,#6448,#6449);
#5492=AXIS2_PLACEMENT_3D('',#7962,#6451,#6452);
#5493=AXIS2_PLACEMENT_3D('',#7964,#6453,#6454);
#5494=AXIS2_PLACEMENT_3D('',#7965,#6455,#6456);
#5495=AXIS2_PLACEMENT_3D('',#7967,#6457,#6458);
#5496=AXIS2_PLACEMENT_3D('',#7969,#6460,#6461);
#6392=DIRECTION('axis',(0.,0.,1.));
#6393=DIRECTION('refdir',(1.,0.,0.));
#6394=DIRECTION('center_axis',(0.866025403784439,0.,-0.5));
#6395=DIRECTION('ref_axis',(0.5,0.,0.866025403784439));
#6396=DIRECTION('',(-0.5,0.,-0.866025403784439));
#6397=DIRECTION('',(0.,-1.,0.));
#6398=DIRECTION('',(0.5,0.,0.866025403784439));
#6399=DIRECTION('',(0.,-1.,0.));
#6400=DIRECTION('center_axis',(1.20185167898973E-16,0.,-1.));
#6401=DIRECTION('ref_axis',(1.,0.,1.20185167898973E-16));
#6402=DIRECTION('',(-1.,0.,-1.20185167898973E-16));
#6403=DIRECTION('',(0.,-1.,0.));
#6404=DIRECTION('',(1.,0.,1.20185167898973E-16));
#6405=DIRECTION('center_axis',(-0.866025403784439,0.,-0.5));
#6406=DIRECTION('ref_axis',(0.5,0.,-0.866025403784439));
#6407=DIRECTION('',(-0.5,0.,0.866025403784439));
#6408=DIRECTION('',(0.,-1.,0.));
#6409=DIRECTION('',(0.5,0.,-0.866025403784439));
#6410=DIRECTION('center_axis',(-0.866025403784439,0.,0.5));
#6411=DIRECTION('ref_axis',(-0.5,0.,-0.866025403784439));
#6412=DIRECTION('',(0.5,0.,0.866025403784439));
#6413=DIRECTION('',(0.,-1.,0.));
#6414=DIRECTION('',(-0.5,0.,-0.866025403784439));
#6415=DIRECTION('center_axis',(-2.40370335797945E-16,0.,1.));
#6416=DIRECTION('ref_axis',(-1.,0.,-2.40370335797945E-16));
#6417=DIRECTION('',(1.,0.,2.40370335797945E-16));
#6418=DIRECTION('',(0.,-1.,0.));
#6419=DIRECTION('',(-1.,0.,-2.40370335797945E-16));
#6420=DIRECTION('center_axis',(0.866025403784439,0.,0.5));
#6421=DIRECTION('ref_axis',(-0.5,0.,0.866025403784439));
#6422=DIRECTION('',(0.5,0.,-0.866025403784439));
#6423=DIRECTION('',(-0.5,0.,0.866025403784439));
#6424=DIRECTION('center_axis',(0.,1.,0.));
#6425=DIRECTION('ref_axis',(1.,0.,0.));
#6426=DIRECTION('center_axis',(0.,-1.,0.));
#6427=DIRECTION('ref_axis',(0.,0.,-1.));
#6428=DIRECTION('center_axis',(0.,1.,0.));
#6429=DIRECTION('ref_axis',(1.,0.,0.));
#6430=DIRECTION('center_axis',(0.,1.,0.));
#6431=DIRECTION('ref_axis',(1.,0.,0.));
#6432=DIRECTION('center_axis',(0.,1.,0.));
#6433=DIRECTION('ref_axis',(0.,0.,1.));
#6434=DIRECTION('center_axis',(0.,-1.,0.));
#6435=DIRECTION('ref_axis',(1.,0.,0.));
#6436=DIRECTION('center_axis',(0.,-1.,0.));
#6437=DIRECTION('ref_axis',(1.,0.,0.));
#6438=DIRECTION('center_axis',(0.,-1.,0.));
#6439=DIRECTION('ref_axis',(1.,0.,0.));
#6440=DIRECTION('',(0.707106781186548,0.707106781186547,8.65956056235493E-17));
#6441=DIRECTION('center_axis',(0.,-1.,0.));
#6442=DIRECTION('ref_axis',(1.,0.,0.));
#6443=DIRECTION('center_axis',(0.,-1.,0.));
#6444=DIRECTION('ref_axis',(1.,0.,0.));
#6445=DIRECTION('',(0.,1.,0.));
#6446=DIRECTION('center_axis',(0.,1.,0.));
#6447=DIRECTION('ref_axis',(1.,0.,0.));
#6448=DIRECTION('center_axis',(0.,-1.,0.));
#6449=DIRECTION('ref_axis',(1.,0.,0.));
#6450=DIRECTION('',(-0.707106781186547,0.707106781186548,-8.65956056235493E-17));
#6451=DIRECTION('center_axis',(0.,-1.,0.));
#6452=DIRECTION('ref_axis',(0.,0.,-1.));
#6453=DIRECTION('center_axis',(0.,-1.,0.));
#6454=DIRECTION('ref_axis',(1.,0.,0.));
#6455=DIRECTION('center_axis',(0.,1.,0.));
#6456=DIRECTION('ref_axis',(1.,0.,0.));
#6457=DIRECTION('center_axis',(0.,1.,0.));
#6458=DIRECTION('ref_axis',(1.,0.,0.));
#6459=DIRECTION('',(-0.447213595499958,0.894427190999916,-5.47678698264203E-17));
#6460=DIRECTION('center_axis',(0.,-1.,0.));
#6461=DIRECTION('ref_axis',(1.,0.,0.));
#6462=DIRECTION('',(0.,1.,0.));
#7905=CARTESIAN_POINT('',(0.,0.,0.));
#7906=CARTESIAN_POINT('Origin',(0.115470053837925,-0.5,-0.2));
#7907=CARTESIAN_POINT('',(0.23094010767585,-0.5,0.));
#7908=CARTESIAN_POINT('',(0.115470053837925,-0.5,-0.2));
#7909=CARTESIAN_POINT('',(0.23094010767585,-0.5,0.));
#7910=CARTESIAN_POINT('',(0.115470053837925,-0.8,-0.2));
#7911=CARTESIAN_POINT('',(0.115470053837925,-0.5,-0.2));
#7912=CARTESIAN_POINT('',(0.23094010767585,-0.8,0.));
#7913=CARTESIAN_POINT('',(0.23094010767585,-0.8,0.));
#7914=CARTESIAN_POINT('',(0.23094010767585,-0.5,0.));
#7915=CARTESIAN_POINT('Origin',(-0.115470053837925,-0.5,-0.2));
#7916=CARTESIAN_POINT('',(-0.115470053837925,-0.5,-0.2));
#7917=CARTESIAN_POINT('',(0.115470053837925,-0.5,-0.2));
#7918=CARTESIAN_POINT('',(-0.115470053837925,-0.8,-0.2));
#7919=CARTESIAN_POINT('',(-0.115470053837925,-0.5,-0.2));
#7920=CARTESIAN_POINT('',(0.115470053837925,-0.8,-0.2));
#7921=CARTESIAN_POINT('Origin',(-0.23094010767585,-0.5,-2.77555756156289E-17));
#7922=CARTESIAN_POINT('',(-0.23094010767585,-0.5,-2.82820063659975E-17));
#7923=CARTESIAN_POINT('',(-0.115470053837925,-0.5,-0.2));
#7924=CARTESIAN_POINT('',(-0.23094010767585,-0.8,-2.77555756156289E-17));
#7925=CARTESIAN_POINT('',(-0.23094010767585,-0.5,-2.82820063659975E-17));
#7926=CARTESIAN_POINT('',(-0.115470053837925,-0.8,-0.2));
#7927=CARTESIAN_POINT('Origin',(-0.115470053837925,-0.5,0.2));
#7928=CARTESIAN_POINT('',(-0.115470053837925,-0.5,0.2));
#7929=CARTESIAN_POINT('',(-0.23094010767585,-0.5,-2.82820063659975E-17));
#7930=CARTESIAN_POINT('',(-0.115470053837925,-0.8,0.2));
#7931=CARTESIAN_POINT('',(-0.115470053837925,-0.5,0.2));
#7932=CARTESIAN_POINT('',(-0.23094010767585,-0.8,-2.82820063659975E-17));
#7933=CARTESIAN_POINT('Origin',(0.115470053837925,-0.5,0.2));
#7934=CARTESIAN_POINT('',(0.115470053837925,-0.5,0.2));
#7935=CARTESIAN_POINT('',(-0.115470053837925,-0.5,0.2));
#7936=CARTESIAN_POINT('',(0.115470053837925,-0.8,0.2));
#7937=CARTESIAN_POINT('',(0.115470053837925,-0.5,0.2));
#7938=CARTESIAN_POINT('',(-0.115470053837925,-0.8,0.2));
#7939=CARTESIAN_POINT('Origin',(0.23094010767585,-0.5,0.));
#7940=CARTESIAN_POINT('',(0.115470053837925,-0.5,0.2));
#7941=CARTESIAN_POINT('',(0.115470053837925,-0.8,0.2));
#7942=CARTESIAN_POINT('Origin',(0.,-0.5,0.));
#7943=CARTESIAN_POINT('Origin',(0.,-0.8,0.));
#7944=CARTESIAN_POINT('Origin',(0.,-1.4,0.));
#7945=CARTESIAN_POINT('',(-0.24505,-1.4,3.00099698131059E-17));
#7946=CARTESIAN_POINT('Origin',(0.,-1.4,0.));
#7947=CARTESIAN_POINT('Origin',(0.375,0.5,0.));
#7948=CARTESIAN_POINT('',(-0.375,0.5,-4.59242549680257E-17));
#7949=CARTESIAN_POINT('Origin',(0.,0.5,0.));
#7950=CARTESIAN_POINT('Origin',(0.,0.475,0.));
#7951=CARTESIAN_POINT('',(-0.425,0.45,-5.20474889637625E-17));
#7952=CARTESIAN_POINT('Origin',(0.,0.45,0.));
#7953=CARTESIAN_POINT('',(-0.4,0.475,-4.89858719658941E-17));
#7954=CARTESIAN_POINT('Origin',(0.,0.24,0.));
#7955=CARTESIAN_POINT('',(-0.425,0.0299999999999998,-5.20474889637625E-17));
#7956=CARTESIAN_POINT('Origin',(0.,0.0299999999999998,0.));
#7957=CARTESIAN_POINT('',(-0.425,0.24,-5.20474889637625E-17));
#7958=CARTESIAN_POINT('Origin',(0.,0.0150000000000001,0.));
#7959=CARTESIAN_POINT('',(-0.395,4.85722573273506E-17,-4.83735485663204E-17));
#7960=CARTESIAN_POINT('Origin',(0.,0.,0.));
#7961=CARTESIAN_POINT('',(-0.41,0.0150000000000001,-5.02105187650415E-17));
#7962=CARTESIAN_POINT('Origin',(0.27,0.,0.));
#7963=CARTESIAN_POINT('',(-0.27,0.,-3.30654635769785E-17));
#7964=CARTESIAN_POINT('Origin',(0.,0.,0.));
#7965=CARTESIAN_POINT('Origin',(0.,-0.02,0.));
#7966=CARTESIAN_POINT('',(-0.24505,-0.0498999999999999,3.00099698131059E-17));
#7967=CARTESIAN_POINT('Origin',(0.,-0.0498999999999999,0.));
#7968=CARTESIAN_POINT('',(-0.26,-0.02,-3.18408167778312E-17));
#7969=CARTESIAN_POINT('Origin',(0.,-0.995,0.));
#7970=CARTESIAN_POINT('',(-0.24505,-0.995,-3.00099698131059E-17));
#10246=UNCERTAINTY_MEASURE_WITH_UNIT(LENGTH_MEASURE(0.001),#10293,
'DISTANCE_ACCURACY_VALUE',
'Maximum model space distance between geometric entities at asserted c
onnectivities');
#10264=UNCERTAINTY_MEASURE_WITH_UNIT(LENGTH_MEASURE(0.001),#10293,
'DISTANCE_ACCURACY_VALUE',
'Maximum model space distance between geometric entities at asserted c
onnectivities');
#10274=(
GEOMETRIC_REPRESENTATION_CONTEXT(3)
GLOBAL_UNCERTAINTY_ASSIGNED_CONTEXT((#10246))
GLOBAL_UNIT_ASSIGNED_CONTEXT((#10293,#10295,#10296))
REPRESENTATION_CONTEXT('','3D')
);
#10292=(
GEOMETRIC_REPRESENTATION_CONTEXT(3)
GLOBAL_UNCERTAINTY_ASSIGNED_CONTEXT((#10264))
GLOBAL_UNIT_ASSIGNED_CONTEXT((#10293,#10295,#10296))
REPRESENTATION_CONTEXT('','3D')
);
#10293=(
LENGTH_UNIT()
NAMED_UNIT(*)
SI_UNIT(.CENTI.,.METRE.)
);
#10295=(
NAMED_UNIT(*)
PLANE_ANGLE_UNIT()
SI_UNIT($,.RADIAN.)
);
#10296=(
NAMED_UNIT(*)
SI_UNIT($,.STERADIAN.)
SOLID_ANGLE_UNIT()
);
#10306=SHAPE_DEFINITION_REPRESENTATION(#10333,#10422);
#10333=PRODUCT_DEFINITION_SHAPE('',$,#10450);
#10422=SHAPE_REPRESENTATION('',(#5473),#10274);
#10440=PRODUCT_DEFINITION_CONTEXT('part definition',#10523,'design');
#10450=PRODUCT_DEFINITION('M5x14 Cap Screw (1)',
'M5x14 Cap Screw (1)',#10477,#10440);
#10477=PRODUCT_DEFINITION_FORMATION('',$,#10534);
#10523=APPLICATION_CONTEXT(
'Core Data for Automotive Mechanical Design Process');
#10524=PRODUCT_CONTEXT('part definition',#10523,'mechanical');
#10534=PRODUCT('M5x14 Cap Screw (1)','M5x14 Cap Screw (1)',
'M5x14 Cap Screw (1)',(#10524));
#10629=COLOUR_RGB('Black',0.12,0.14,0.17);
#10630=FILL_AREA_STYLE_COLOUR('',#10629);
#10631=FILL_AREA_STYLE('',(#10630));
#10632=SURFACE_STYLE_FILL_AREA(#10631);
#10633=SURFACE_SIDE_STYLE('',(#10632));
#10634=SURFACE_STYLE_USAGE(.BOTH.,#10633);
#10635=PRESENTATION_STYLE_ASSIGNMENT((#10634));
ENDSEC;
END-ISO-10303-21;
